ISO-10303-21;
HEADER;
/* Generated by software containing ST-Developer
 * from STEP Tools, Inc. (www.steptools.com) 
 */

FILE_DESCRIPTION(
/* description */ ('Bin tilter linkage'),
/* implementation_level */ '2;1');

FILE_NAME(
/* name */ 'M4 short cap screw (13).step',
/* time_stamp */ '2026-10-28T03:26:24-07:00',
/* author */ (''),
/* organization */ (''),
/* preprocessor_version */ 'ST-DEVELOPER v20.2',
/* originating_system */ 'Autodesk Translation Framework v15.17.0.0',
/* authorisation */ '');

FILE_SCHEMA (('AUTOMOTIVE_DESIGN { 1 0 10303 214 3 1 1 }'));
ENDSEC;

DATA;
#10=MECHANICAL_DESIGN_GEOMETRIC_PRESENTATION_REPRESENTATION('',(#910),#23728);
#698=SHAPE_REPRESENTATION_RELATIONSHIP('SRR','None',#24163,#804);
#804=ADVANCED_BREP_SHAPE_REPRESENTATION('',(#1023),#23663);
#910=STYLED_ITEM('',(#24772),#1023);
#1023=MANIFOLD_SOLID_BREP('Body1',#12441);
#1307=FACE_BOUND('',#3250,.T.);
#1668=PLANE('',#14458);
#1669=PLANE('',#14463);
#1670=PLANE('',#14466);
#2252=FACE_OUTER_BOUND('',#3249,.T.);
#2253=FACE_OUTER_BOUND('',#3251,.T.);
#2254=FACE_OUTER_BOUND('',#3252,.T.);
#2255=FACE_OUTER_BOUND('',#3253,.T.);
#2256=FACE_OUTER_BOUND('',#3254,.T.);
#3249=EDGE_LOOP('',(#9757));
#3250=EDGE_LOOP('',(#9758));
#3251=EDGE_LOOP('',(#9759,#9760,#9761,#9762));
#3252=EDGE_LOOP('',(#9763));
#3253=EDGE_LOOP('',(#9764,#9765,#9766,#9767));
#3254=EDGE_LOOP('',(#9768));
#4173=LINE('',#21319,#4848);
#4174=LINE('',#21323,#4849);
#4848=VECTOR('',#17372,0.35);
#4849=VECTOR('',#17377,0.199999999999999);
#5567=CIRCLE('',#14459,0.35);
#5568=CIRCLE('',#14460,0.199999999999999);
#5569=CIRCLE('',#14462,0.35);
#5570=CIRCLE('',#14465,0.199999999999999);
#6417=VERTEX_POINT('',#21312);
#6418=VERTEX_POINT('',#21314);
#6419=VERTEX_POINT('',#21317);
#6420=VERTEX_POINT('',#21322);
#7618=EDGE_CURVE('',#6417,#6417,#5567,.T.);
#7619=EDGE_CURVE('',#6418,#6418,#5568,.T.);
#7620=EDGE_CURVE('',#6419,#6419,#5569,.T.);
#7621=EDGE_CURVE('',#6419,#6417,#4173,.T.);
#7622=EDGE_CURVE('',#6418,#6420,#4174,.T.);
#7623=EDGE_CURVE('',#6420,#6420,#5570,.T.);
#9757=ORIENTED_EDGE('',*,*,#7618,.F.);
#9758=ORIENTED_EDGE('',*,*,#7619,.T.);
#9759=ORIENTED_EDGE('',*,*,#7620,.F.);
#9760=ORIENTED_EDGE('',*,*,#7621,.T.);
#9761=ORIENTED_EDGE('',*,*,#7618,.T.);
#9762=ORIENTED_EDGE('',*,*,#7621,.F.);
#9763=ORIENTED_EDGE('',*,*,#7620,.T.);
#9764=ORIENTED_EDGE('',*,*,#7619,.F.);
#9765=ORIENTED_EDGE('',*,*,#7622,.T.);
#9766=ORIENTED_EDGE('',*,*,#7623,.T.);
#9767=ORIENTED_EDGE('',*,*,#7622,.F.);
#9768=ORIENTED_EDGE('',*,*,#7623,.F.);
#11449=CYLINDRICAL_SURFACE('',#14461,0.35);
#11450=CYLINDRICAL_SURFACE('',#14464,0.199999999999999);
#11977=ADVANCED_FACE('',(#2252,#1307),#1668,.F.);
#11978=ADVANCED_FACE('',(#2253),#11449,.T.);
#11979=ADVANCED_FACE('',(#2254),#1669,.T.);
#11980=ADVANCED_FACE('',(#2255),#11450,.T.);
#11981=ADVANCED_FACE('',(#2256),#1670,.F.);
#12441=CLOSED_SHELL('',(#11977,#11978,#11979,#11980,#11981));
#14457=AXIS2_PLACEMENT_3D('',#21310,#17360,#17361);
#14458=AXIS2_PLACEMENT_3D('',#21311,#17362,#17363);
#14459=AXIS2_PLACEMENT_3D('',#21313,#17364,#17365);
#14460=AXIS2_PLACEMENT_3D('',#21315,#17366,#17367);
#14461=AXIS2_PLACEMENT_3D('',#21316,#17368,#17369);
#14462=AXIS2_PLACEMENT_3D('',#21318,#17370,#17371);
#14463=AXIS2_PLACEMENT_3D('',#21320,#17373,#17374);
#14464=AXIS2_PLACEMENT_3D('',#21321,#17375,#17376);
#14465=AXIS2_PLACEMENT_3D('',#21324,#17378,#17379);
#14466=AXIS2_PLACEMENT_3D('',#21325,#17380,#17381);
#17360=DIRECTION('axis',(0.,0.,1.));
#17361=DIRECTION('refdir',(1.,0.,0.));
#17362=DIRECTION('center_axis',(0.,1.,0.));
#17363=DIRECTION('ref_axis',(1.,0.,0.));
#17364=DIRECTION('center_axis',(0.,1.,0.));
#17365=DIRECTION('ref_axis',(1.,0.,0.));
#17366=DIRECTION('center_axis',(0.,1.,0.));
#17367=DIRECTION('ref_axis',(1.,0.,0.));
#17368=DIRECTION('center_axis',(0.,1.,0.));
#17369=DIRECTION('ref_axis',(1.,0.,0.));
#17370=DIRECTION('center_axis',(0.,1.,0.));
#17371=DIRECTION('ref_axis',(1.,0.,0.));
#17372=DIRECTION('',(0.,-1.,0.));
#17373=DIRECTION('center_axis',(0.,1.,0.));
#17374=DIRECTION('ref_axis',(1.,0.,0.));
#17375=DIRECTION('center_axis',(0.,1.,0.));
#17376=DIRECTION('ref_axis',(1.,0.,0.));
#17377=DIRECTION('',(0.,-1.,0.));
#17378=DIRECTION('center_axis',(0.,1.,0.));
#17379=DIRECTION('ref_axis',(1.,0.,0.));
#17380=DIRECTION('center_axis',(0.,1.,0.));
#17381=DIRECTION('ref_axis',(1.,0.,0.));
#21310=CARTESIAN_POINT('',(0.,0.,0.));
#21311=CARTESIAN_POINT('Origin',(8.08877866266397,0.8,19.7283489784518));
#21312=CARTESIAN_POINT('',(7.73877866266397,0.8,19.7283489784518));
#21313=CARTESIAN_POINT('Origin',(8.08877866266397,0.8,19.7283489784518));
#21314=CARTESIAN_POINT('',(7.88877866266397,0.8,19.7283489784518));
#21315=CARTESIAN_POINT('Origin',(8.08877866266397,0.8,19.7283489784518));
#21316=CARTESIAN_POINT('Origin',(8.08877866266397,0.8,19.7283489784518));
#21317=CARTESIAN_POINT('',(7.73877866266397,1.2,19.7283489784518));
#21318=CARTESIAN_POINT('Origin',(8.08877866266397,1.2,19.7283489784518));
#21319=CARTESIAN_POINT('',(7.73877866266397,0.8,19.7283489784518));
#21320=CARTESIAN_POINT('Origin',(8.08877866266397,1.2,19.7283489784518));
#21321=CARTESIAN_POINT('Origin',(8.08877866266397,0.1,19.7283489784518));
#21322=CARTESIAN_POINT('',(7.88877866266397,0.1,19.7283489784518));
#21323=CARTESIAN_POINT('',(7.88877866266397,0.1,19.7283489784518));
#21324=CARTESIAN_POINT('Origin',(8.08877866266397,0.1,19.7283489784518));
#21325=CARTESIAN_POINT('Origin',(8.08877866266397,0.1,19.7283489784518));
#23546=UNCERTAINTY_MEASURE_WITH_UNIT(LENGTH_MEASURE(0.001),#23729,
'DISTANCE_ACCURACY_VALUE',
'Maximum model space distance between geometric entities at asserted c
onnectivities');
#23611=UNCERTAINTY_MEASURE_WITH_UNIT(LENGTH_MEASURE(0.001),#23729,
'DISTANCE_ACCURACY_VALUE',
'Maximum model space distance between geometric entities at asserted c
onnectivities');
#23663=(
GEOMETRIC_REPRESENTATION_CONTEXT(3)
GLOBAL_UNCERTAINTY_ASSIGNED_CONTEXT((#23546))
GLOBAL_UNIT_ASSIGNED_CONTEXT((#23729,#23731,#23732))
REPRESENTATION_CONTEXT('','3D')
);
#23728=(
GEOMETRIC_REPRESENTATION_CONTEXT(3)
GLOBAL_UNCERTAINTY_ASSIGNED_CONTEXT((#23611))
GLOBAL_UNIT_ASSIGNED_CONTEXT((#23729,#23731,#23732))
REPRESENTATION_CONTEXT('','3D')
);
#23729=(
LENGTH_UNIT()
NAMED_UNIT(*)
SI_UNIT(.CENTI.,.METRE.)
);
#23731=(
NAMED_UNIT(*)
PLANE_ANGLE_UNIT()
SI_UNIT($,.RADIAN.)
);
#23732=(
NAMED_UNIT(*)
SI_UNIT($,.STERADIAN.)
SOLID_ANGLE_UNIT()
);
#23784=SHAPE_DEFINITION_REPRESENTATION(#23900,#24163);
#23900=PRODUCT_DEFINITION_SHAPE('',$,#24280);
#24163=SHAPE_REPRESENTATION('',(#14457),#23663);
#24228=PRODUCT_DEFINITION_CONTEXT('part definition',#24578,'design');
#24280=PRODUCT_DEFINITION('M4 short cap screw (13)',
'M4 short cap screw (13)',#24396,#24228);
#24396=PRODUCT_DEFINITION_FORMATION('',$,#24631);
#24578=APPLICATION_CONTEXT(
'Core Data for Automotive Mechanical Design Process');
#24579=PRODUCT_CONTEXT('part definition',#24578,'mechanical');
#24631=PRODUCT('M4 short cap screw (13)','M4 short cap screw (13)',
'M4 short cap screw (13)',(#24579));
#24766=COLOUR_RGB('Black',0.12,0.14,0.17);
#24767=FILL_AREA_STYLE_COLOUR('',#24766);
#24768=FILL_AREA_STYLE('',(#24767));
#24769=SURFACE_STYLE_FILL_AREA(#24768);
#24770=SURFACE_SIDE_STYLE('',(#24769));
#24771=SURFACE_STYLE_USAGE(.BOTH.,#24770);
#24772=PRESENTATION_STYLE_ASSIGNMENT((#24771));
ENDSEC;
END-ISO-10303-21;
